ISO-10303-21;
HEADER;
/* Generated by software containing ST-Developer
 * from STEP Tools, Inc. (www.steptools.com) 
 */

FILE_DESCRIPTION(
/* description */ ('Cam-and-follower valve demonstrator'),
/* implementation_level */ '2;1');

FILE_NAME(
/* name */ 'Bearing cap (2).step',
/* time_stamp */ '2026-10-28T03:25:17-07:00',
/* author */ (''),
/* organization */ (''),
/* preprocessor_version */ 'ST-DEVELOPER v20.2',
/* originating_system */ 'Autodesk Translation Framework v15.17.0.0',
/* authorisation */ '');

FILE_SCHEMA (('AUTOMOTIVE_DESIGN { 1 0 10303 214 3 1 1 }'));
ENDSEC;

DATA;
#10=MECHANICAL_DESIGN_GEOMETRIC_PRESENTATION_REPRESENTATION('',(#419),#12896);
#347=SHAPE_REPRESENTATION_RELATIONSHIP('SRR','None',#13063,#383);
#383=ADVANCED_BREP_SHAPE_REPRESENTATION('',(#462),#12863);
#419=STYLED_ITEM('',(#13330),#462);
#462=MANIFOLD_SOLID_BREP('Body1',#6186);
#558=FACE_BOUND('',#1615,.T.);
#559=FACE_BOUND('',#1619,.T.);
#560=FACE_BOUND('',#1620,.T.);
#561=FACE_BOUND('',#1621,.T.);
#562=FACE_BOUND('',#1622,.T.);
#563=FACE_BOUND('',#1623,.T.);
#564=FACE_BOUND('',#1625,.T.);
#565=FACE_BOUND('',#1626,.T.);
#566=FACE_BOUND('',#1627,.T.);
#567=FACE_BOUND('',#1628,.T.);
#568=FACE_BOUND('',#1629,.T.);
#727=CIRCLE('',#6784,0.225);
#728=CIRCLE('',#6785,0.225);
#729=CIRCLE('',#6787,0.225);
#730=CIRCLE('',#6788,0.225);
#731=CIRCLE('',#6790,0.225);
#732=CIRCLE('',#6791,0.225);
#733=CIRCLE('',#6793,0.225);
#734=CIRCLE('',#6794,0.225);
#735=CIRCLE('',#6796,1.59);
#736=CIRCLE('',#6797,1.59);
#737=CIRCLE('',#6799,1.005);
#738=CIRCLE('',#6801,1.005);
#739=CIRCLE('',#6803,2.4);
#740=CIRCLE('',#6804,2.4);
#1007=CYLINDRICAL_SURFACE('',#6783,0.225);
#1008=CYLINDRICAL_SURFACE('',#6786,0.225);
#1009=CYLINDRICAL_SURFACE('',#6789,0.225);
#1010=CYLINDRICAL_SURFACE('',#6792,0.225);
#1011=CYLINDRICAL_SURFACE('',#6795,1.59);
#1012=CYLINDRICAL_SURFACE('',#6800,1.005);
#1013=CYLINDRICAL_SURFACE('',#6802,2.4);
#1178=FACE_OUTER_BOUND('',#1609,.T.);
#1179=FACE_OUTER_BOUND('',#1610,.T.);
#1180=FACE_OUTER_BOUND('',#1611,.T.);
#1181=FACE_OUTER_BOUND('',#1612,.T.);
#1182=FACE_OUTER_BOUND('',#1613,.T.);
#1183=FACE_OUTER_BOUND('',#1614,.T.);
#1184=FACE_OUTER_BOUND('',#1616,.T.);
#1185=FACE_OUTER_BOUND('',#1617,.T.);
#1186=FACE_OUTER_BOUND('',#1618,.T.);
#1187=FACE_OUTER_BOUND('',#1624,.T.);
#1609=EDGE_LOOP('',(#4491,#4492,#4493,#4494));
#1610=EDGE_LOOP('',(#4495,#4496,#4497,#4498));
#1611=EDGE_LOOP('',(#4499,#4500,#4501,#4502));
#1612=EDGE_LOOP('',(#4503,#4504,#4505,#4506));
#1613=EDGE_LOOP('',(#4507,#4508,#4509,#4510));
#1614=EDGE_LOOP('',(#4511));
#1615=EDGE_LOOP('',(#4512));
#1616=EDGE_LOOP('',(#4513,#4514,#4515,#4516));
#1617=EDGE_LOOP('',(#4517,#4518,#4519,#4520));
#1618=EDGE_LOOP('',(#4521));
#1619=EDGE_LOOP('',(#4522));
#1620=EDGE_LOOP('',(#4523));
#1621=EDGE_LOOP('',(#4524));
#1622=EDGE_LOOP('',(#4525));
#1623=EDGE_LOOP('',(#4526));
#1624=EDGE_LOOP('',(#4527));
#1625=EDGE_LOOP('',(#4528));
#1626=EDGE_LOOP('',(#4529));
#1627=EDGE_LOOP('',(#4530));
#1628=EDGE_LOOP('',(#4531));
#1629=EDGE_LOOP('',(#4532));
#2125=LINE('',#9847,#2547);
#2126=LINE('',#9853,#2548);
#2127=LINE('',#9859,#2549);
#2128=LINE('',#9865,#2550);
#2129=LINE('',#9871,#2551);
#2130=LINE('',#9878,#2552);
#2131=LINE('',#9884,#2553);
#2547=VECTOR('',#7870,0.225);
#2548=VECTOR('',#7877,0.225);
#2549=VECTOR('',#7884,0.225);
#2550=VECTOR('',#7891,0.225);
#2551=VECTOR('',#7898,1.59);
#2552=VECTOR('',#7907,1.005);
#2553=VECTOR('',#7914,2.4);
#2971=VERTEX_POINT('',#9844);
#2972=VERTEX_POINT('',#9846);
#2973=VERTEX_POINT('',#9850);
#2974=VERTEX_POINT('',#9852);
#2975=VERTEX_POINT('',#9856);
#2976=VERTEX_POINT('',#9858);
#2977=VERTEX_POINT('',#9862);
#2978=VERTEX_POINT('',#9864);
#2979=VERTEX_POINT('',#9868);
#2980=VERTEX_POINT('',#9870);
#2981=VERTEX_POINT('',#9874);
#2982=VERTEX_POINT('',#9877);
#2983=VERTEX_POINT('',#9881);
#2984=VERTEX_POINT('',#9883);
#3542=EDGE_CURVE('',#2971,#2971,#727,.T.);
#3543=EDGE_CURVE('',#2971,#2972,#2125,.T.);
#3544=EDGE_CURVE('',#2972,#2972,#728,.T.);
#3545=EDGE_CURVE('',#2973,#2973,#729,.T.);
#3546=EDGE_CURVE('',#2973,#2974,#2126,.T.);
#3547=EDGE_CURVE('',#2974,#2974,#730,.T.);
#3548=EDGE_CURVE('',#2975,#2975,#731,.T.);
#3549=EDGE_CURVE('',#2975,#2976,#2127,.T.);
#3550=EDGE_CURVE('',#2976,#2976,#732,.T.);
#3551=EDGE_CURVE('',#2977,#2977,#733,.T.);
#3552=EDGE_CURVE('',#2977,#2978,#2128,.T.);
#3553=EDGE_CURVE('',#2978,#2978,#734,.T.);
#3554=EDGE_CURVE('',#2979,#2979,#735,.T.);
#3555=EDGE_CURVE('',#2979,#2980,#2129,.T.);
#3556=EDGE_CURVE('',#2980,#2980,#736,.T.);
#3557=EDGE_CURVE('',#2981,#2981,#737,.T.);
#3558=EDGE_CURVE('',#2981,#2982,#2130,.T.);
#3559=EDGE_CURVE('',#2982,#2982,#738,.T.);
#3560=EDGE_CURVE('',#2983,#2983,#739,.T.);
#3561=EDGE_CURVE('',#2983,#2984,#2131,.T.);
#3562=EDGE_CURVE('',#2984,#2984,#740,.T.);
#4491=ORIENTED_EDGE('',*,*,#3542,.F.);
#4492=ORIENTED_EDGE('',*,*,#3543,.T.);
#4493=ORIENTED_EDGE('',*,*,#3544,.F.);
#4494=ORIENTED_EDGE('',*,*,#3543,.F.);
#4495=ORIENTED_EDGE('',*,*,#3545,.F.);
#4496=ORIENTED_EDGE('',*,*,#3546,.T.);
#4497=ORIENTED_EDGE('',*,*,#3547,.F.);
#4498=ORIENTED_EDGE('',*,*,#3546,.F.);
#4499=ORIENTED_EDGE('',*,*,#3548,.F.);
#4500=ORIENTED_EDGE('',*,*,#3549,.T.);
#4501=ORIENTED_EDGE('',*,*,#3550,.F.);
#4502=ORIENTED_EDGE('',*,*,#3549,.F.);
#4503=ORIENTED_EDGE('',*,*,#3551,.F.);
#4504=ORIENTED_EDGE('',*,*,#3552,.T.);
#4505=ORIENTED_EDGE('',*,*,#3553,.F.);
#4506=ORIENTED_EDGE('',*,*,#3552,.F.);
#4507=ORIENTED_EDGE('',*,*,#3554,.F.);
#4508=ORIENTED_EDGE('',*,*,#3555,.T.);
#4509=ORIENTED_EDGE('',*,*,#3556,.F.);
#4510=ORIENTED_EDGE('',*,*,#3555,.F.);
#4511=ORIENTED_EDGE('',*,*,#3554,.T.);
#4512=ORIENTED_EDGE('',*,*,#3557,.T.);
#4513=ORIENTED_EDGE('',*,*,#3557,.F.);
#4514=ORIENTED_EDGE('',*,*,#3558,.T.);
#4515=ORIENTED_EDGE('',*,*,#3559,.T.);
#4516=ORIENTED_EDGE('',*,*,#3558,.F.);
#4517=ORIENTED_EDGE('',*,*,#3560,.F.);
#4518=ORIENTED_EDGE('',*,*,#3561,.T.);
#4519=ORIENTED_EDGE('',*,*,#3562,.T.);
#4520=ORIENTED_EDGE('',*,*,#3561,.F.);
#4521=ORIENTED_EDGE('',*,*,#3560,.T.);
#4522=ORIENTED_EDGE('',*,*,#3556,.T.);
#4523=ORIENTED_EDGE('',*,*,#3553,.T.);
#4524=ORIENTED_EDGE('',*,*,#3550,.T.);
#4525=ORIENTED_EDGE('',*,*,#3547,.T.);
#4526=ORIENTED_EDGE('',*,*,#3544,.T.);
#4527=ORIENTED_EDGE('',*,*,#3562,.F.);
#4528=ORIENTED_EDGE('',*,*,#3559,.F.);
#4529=ORIENTED_EDGE('',*,*,#3551,.T.);
#4530=ORIENTED_EDGE('',*,*,#3548,.T.);
#4531=ORIENTED_EDGE('',*,*,#3545,.T.);
#4532=ORIENTED_EDGE('',*,*,#3542,.T.);
#5646=PLANE('',#6798);
#5647=PLANE('',#6805);
#5648=PLANE('',#6806);
#5894=ADVANCED_FACE('',(#1178),#1007,.F.);
#5895=ADVANCED_FACE('',(#1179),#1008,.F.);
#5896=ADVANCED_FACE('',(#1180),#1009,.F.);
#5897=ADVANCED_FACE('',(#1181),#1010,.F.);
#5898=ADVANCED_FACE('',(#1182),#1011,.T.);
#5899=ADVANCED_FACE('',(#1183,#558),#5646,.T.);
#5900=ADVANCED_FACE('',(#1184),#1012,.F.);
#5901=ADVANCED_FACE('',(#1185),#1013,.T.);
#5902=ADVANCED_FACE('',(#1186,#559,#560,#561,#562,#563),#5647,.T.);
#5903=ADVANCED_FACE('',(#1187,#564,#565,#566,#567,#568),#5648,.F.);
#6186=CLOSED_SHELL('',(#5894,#5895,#5896,#5897,#5898,#5899,#5900,#5901,
#5902,#5903));
#6782=AXIS2_PLACEMENT_3D('',#9842,#7864,#7865);
#6783=AXIS2_PLACEMENT_3D('',#9843,#7866,#7867);
#6784=AXIS2_PLACEMENT_3D('',#9845,#7868,#7869);
#6785=AXIS2_PLACEMENT_3D('',#9848,#7871,#7872);
#6786=AXIS2_PLACEMENT_3D('',#9849,#7873,#7874);
#6787=AXIS2_PLACEMENT_3D('',#9851,#7875,#7876);
#6788=AXIS2_PLACEMENT_3D('',#9854,#7878,#7879);
#6789=AXIS2_PLACEMENT_3D('',#9855,#7880,#7881);
#6790=AXIS2_PLACEMENT_3D('',#9857,#7882,#7883);
#6791=AXIS2_PLACEMENT_3D('',#9860,#7885,#7886);
#6792=AXIS2_PLACEMENT_3D('',#9861,#7887,#7888);
#6793=AXIS2_PLACEMENT_3D('',#9863,#7889,#7890);
#6794=AXIS2_PLACEMENT_3D('',#9866,#7892,#7893);
#6795=AXIS2_PLACEMENT_3D('',#9867,#7894,#7895);
#6796=AXIS2_PLACEMENT_3D('',#9869,#7896,#7897);
#6797=AXIS2_PLACEMENT_3D('',#9872,#7899,#7900);
#6798=AXIS2_PLACEMENT_3D('',#9873,#7901,#7902);
#6799=AXIS2_PLACEMENT_3D('',#9875,#7903,#7904);
#6800=AXIS2_PLACEMENT_3D('',#9876,#7905,#7906);
#6801=AXIS2_PLACEMENT_3D('',#9879,#7908,#7909);
#6802=AXIS2_PLACEMENT_3D('',#9880,#7910,#7911);
#6803=AXIS2_PLACEMENT_3D('',#9882,#7912,#7913);
#6804=AXIS2_PLACEMENT_3D('',#9885,#7915,#7916);
#6805=AXIS2_PLACEMENT_3D('',#9886,#7917,#7918);
#6806=AXIS2_PLACEMENT_3D('',#9887,#7919,#7920);
#7864=DIRECTION('axis',(0.,0.,1.));
#7865=DIRECTION('refdir',(1.,0.,0.));
#7866=DIRECTION('center_axis',(0.,1.,0.));
#7867=DIRECTION('ref_axis',(1.,0.,0.));
#7868=DIRECTION('center_axis',(0.,1.,0.));
#7869=DIRECTION('ref_axis',(1.,0.,0.));
#7870=DIRECTION('',(0.,1.,0.));
#7871=DIRECTION('center_axis',(0.,-1.,0.));
#7872=DIRECTION('ref_axis',(1.,0.,0.));
#7873=DIRECTION('center_axis',(0.,1.,0.));
#7874=DIRECTION('ref_axis',(1.,0.,0.));
#7875=DIRECTION('center_axis',(0.,1.,0.));
#7876=DIRECTION('ref_axis',(1.,0.,0.));
#7877=DIRECTION('',(0.,1.,0.));
#7878=DIRECTION('center_axis',(0.,-1.,0.));
#7879=DIRECTION('ref_axis',(1.,0.,0.));
#7880=DIRECTION('center_axis',(0.,1.,0.));
#7881=DIRECTION('ref_axis',(1.,0.,0.));
#7882=DIRECTION('center_axis',(0.,1.,0.));
#7883=DIRECTION('ref_axis',(1.,0.,0.));
#7884=DIRECTION('',(0.,1.,0.));
#7885=DIRECTION('center_axis',(0.,-1.,0.));
#7886=DIRECTION('ref_axis',(1.,0.,0.));
#7887=DIRECTION('center_axis',(0.,1.,0.));
#7888=DIRECTION('ref_axis',(1.,0.,0.));
#7889=DIRECTION('center_axis',(0.,1.,0.));
#7890=DIRECTION('ref_axis',(1.,0.,0.));
#7891=DIRECTION('',(0.,1.,0.));
#7892=DIRECTION('center_axis',(0.,-1.,0.));
#7893=DIRECTION('ref_axis',(1.,0.,0.));
#7894=DIRECTION('center_axis',(0.,1.,0.));
#7895=DIRECTION('ref_axis',(1.,0.,0.));
#7896=DIRECTION('center_axis',(0.,1.,0.));
#7897=DIRECTION('ref_axis',(1.,0.,0.));
#7898=DIRECTION('',(0.,-1.,0.));
#7899=DIRECTION('center_axis',(0.,-1.,0.));
#7900=DIRECTION('ref_axis',(1.,0.,0.));
#7901=DIRECTION('center_axis',(0.,1.,0.));
#7902=DIRECTION('ref_axis',(1.,0.,0.));
#7903=DIRECTION('center_axis',(0.,-1.,0.));
#7904=DIRECTION('ref_axis',(1.,0.,0.));
#7905=DIRECTION('center_axis',(0.,1.,0.));
#7906=DIRECTION('ref_axis',(1.,0.,0.));
#7907=DIRECTION('',(0.,-1.,0.));
#7908=DIRECTION('center_axis',(0.,-1.,0.));
#7909=DIRECTION('ref_axis',(1.,0.,0.));
#7910=DIRECTION('center_axis',(0.,1.,0.));
#7911=DIRECTION('ref_axis',(1.,0.,0.));
#7912=DIRECTION('center_axis',(0.,1.,0.));
#7913=DIRECTION('ref_axis',(1.,0.,0.));
#7914=DIRECTION('',(0.,-1.,0.));
#7915=DIRECTION('center_axis',(0.,1.,0.));
#7916=DIRECTION('ref_axis',(1.,0.,0.));
#7917=DIRECTION('center_axis',(0.,1.,0.));
#7918=DIRECTION('ref_axis',(1.,0.,0.));
#7919=DIRECTION('center_axis',(0.,1.,0.));
#7920=DIRECTION('ref_axis',(1.,0.,0.));
#9842=CARTESIAN_POINT('',(0.,0.,0.));
#9843=CARTESIAN_POINT('Origin',(-1.4142135623731,1.4,2.58578643762691));
#9844=CARTESIAN_POINT('',(-1.6392135623731,1.5,2.58578643762691));
#9845=CARTESIAN_POINT('Origin',(-1.4142135623731,1.5,2.58578643762691));
#9846=CARTESIAN_POINT('',(-1.6392135623731,1.7,2.58578643762691));
#9847=CARTESIAN_POINT('',(-1.6392135623731,1.4,2.58578643762691));
#9848=CARTESIAN_POINT('Origin',(-1.4142135623731,1.7,2.58578643762691));
#9849=CARTESIAN_POINT('Origin',(-1.41421356237309,1.4,5.41421356237309));
#9850=CARTESIAN_POINT('',(-1.6392135623731,1.5,5.41421356237309));
#9851=CARTESIAN_POINT('Origin',(-1.41421356237309,1.5,5.41421356237309));
#9852=CARTESIAN_POINT('',(-1.6392135623731,1.7,5.41421356237309));
#9853=CARTESIAN_POINT('',(-1.6392135623731,1.4,5.41421356237309));
#9854=CARTESIAN_POINT('Origin',(-1.41421356237309,1.7,5.41421356237309));
#9855=CARTESIAN_POINT('Origin',(1.4142135623731,1.4,5.41421356237309));
#9856=CARTESIAN_POINT('',(1.1892135623731,1.5,5.41421356237309));
#9857=CARTESIAN_POINT('Origin',(1.4142135623731,1.5,5.41421356237309));
#9858=CARTESIAN_POINT('',(1.1892135623731,1.7,5.41421356237309));
#9859=CARTESIAN_POINT('',(1.1892135623731,1.4,5.41421356237309));
#9860=CARTESIAN_POINT('Origin',(1.4142135623731,1.7,5.41421356237309));
#9861=CARTESIAN_POINT('Origin',(1.41421356237309,1.4,2.5857864376269));
#9862=CARTESIAN_POINT('',(1.18921356237309,1.5,2.5857864376269));
#9863=CARTESIAN_POINT('Origin',(1.41421356237309,1.5,2.5857864376269));
#9864=CARTESIAN_POINT('',(1.18921356237309,1.7,2.5857864376269));
#9865=CARTESIAN_POINT('',(1.18921356237309,1.4,2.5857864376269));
#9866=CARTESIAN_POINT('Origin',(1.41421356237309,1.7,2.5857864376269));
#9867=CARTESIAN_POINT('Origin',(0.,1.7,4.));
#9868=CARTESIAN_POINT('',(-1.59,2.,4.));
#9869=CARTESIAN_POINT('Origin',(0.,2.,4.));
#9870=CARTESIAN_POINT('',(-1.59,1.7,4.));
#9871=CARTESIAN_POINT('',(-1.59,1.7,4.));
#9872=CARTESIAN_POINT('Origin',(0.,1.7,4.));
#9873=CARTESIAN_POINT('Origin',(0.,2.,4.));
#9874=CARTESIAN_POINT('',(-1.005,2.,4.));
#9875=CARTESIAN_POINT('Origin',(0.,2.,4.));
#9876=CARTESIAN_POINT('Origin',(0.,1.5,4.));
#9877=CARTESIAN_POINT('',(-1.005,1.5,4.));
#9878=CARTESIAN_POINT('',(-1.005,1.5,4.));
#9879=CARTESIAN_POINT('Origin',(0.,1.5,4.));
#9880=CARTESIAN_POINT('Origin',(0.,1.5,4.));
#9881=CARTESIAN_POINT('',(-2.4,1.7,4.));
#9882=CARTESIAN_POINT('Origin',(0.,1.7,4.));
#9883=CARTESIAN_POINT('',(-2.4,1.5,4.));
#9884=CARTESIAN_POINT('',(-2.4,1.5,4.));
#9885=CARTESIAN_POINT('Origin',(0.,1.5,4.));
#9886=CARTESIAN_POINT('Origin',(0.,1.7,4.));
#9887=CARTESIAN_POINT('Origin',(0.,1.5,4.));
#12820=UNCERTAINTY_MEASURE_WITH_UNIT(LENGTH_MEASURE(0.001),#12897,
'DISTANCE_ACCURACY_VALUE',
'Maximum model space distance between geometric entities at asserted c
onnectivities');
#12853=UNCERTAINTY_MEASURE_WITH_UNIT(LENGTH_MEASURE(0.001),#12897,
'DISTANCE_ACCURACY_VALUE',
'Maximum model space distance between geometric entities at asserted c
onnectivities');
#12863=(
GEOMETRIC_REPRESENTATION_CONTEXT(3)
GLOBAL_UNCERTAINTY_ASSIGNED_CONTEXT((#12820))
GLOBAL_UNIT_ASSIGNED_CONTEXT((#12897,#12899,#12900))
REPRESENTATION_CONTEXT('','3D')
);
#12896=(
GEOMETRIC_REPRESENTATION_CONTEXT(3)
GLOBAL_UNCERTAINTY_ASSIGNED_CONTEXT((#12853))
GLOBAL_UNIT_ASSIGNED_CONTEXT((#12897,#12899,#12900))
REPRESENTATION_CONTEXT('','3D')
);
#12897=(
LENGTH_UNIT()
NAMED_UNIT(*)
SI_UNIT(.CENTI.,.METRE.)
);
#12899=(
NAMED_UNIT(*)
PLANE_ANGLE_UNIT()
SI_UNIT($,.RADIAN.)
);
#12900=(
NAMED_UNIT(*)
SI_UNIT($,.STERADIAN.)
SOLID_ANGLE_UNIT()
);
#12910=SHAPE_DEFINITION_REPRESENTATION(#12952,#13063);
#12952=PRODUCT_DEFINITION_SHAPE('',$,#13106);
#13063=SHAPE_REPRESENTATION('',(#6782),#12863);
#13096=PRODUCT_DEFINITION_CONTEXT('part definition',#13224,'design');
#13106=PRODUCT_DEFINITION('Bearing cap (2)','Bearing cap (2)',#13148,#13096);
#13148=PRODUCT_DEFINITION_FORMATION('',$,#13235);
#13224=APPLICATION_CONTEXT(
'Core Data for Automotive Mechanical Design Process');
#13225=PRODUCT_CONTEXT('part definition',#13224,'mechanical');
#13235=PRODUCT('Bearing cap (2)','Bearing cap (2)','Bearing cap (2)',(#13225));
#13324=COLOUR_RGB('Grey',0.48,0.52,0.57);
#13325=FILL_AREA_STYLE_COLOUR('',#13324);
#13326=FILL_AREA_STYLE('',(#13325));
#13327=SURFACE_STYLE_FILL_AREA(#13326);
#13328=SURFACE_SIDE_STYLE('',(#13327));
#13329=SURFACE_STYLE_USAGE(.BOTH.,#13328);
#13330=PRESENTATION_STYLE_ASSIGNMENT((#13329));
ENDSEC;
END-ISO-10303-21;
